ISO-10303-21;
HEADER;
FILE_DESCRIPTION (('STEP AP214'),
    '1' );
FILE_NAME ('plain washer hardened small grade a_din_Washer DIN 433 - 17 - 300HV.step',
    '2026-10-09T14:04:53',
    ( '' ),
    ( '' ),
    'SwSTEP 2.0',
    'SolidWorks 2021',
    '' );
FILE_SCHEMA (( 'AUTOMOTIVE_DESIGN' ));
ENDSEC;

DATA;
#405=ORIENTED_EDGE ( 'NONE', *, *, #80496, .T. ) ;
#750=ORIENTED_EDGE ( 'NONE', *, *, #45410, .T. ) ;
#983=UNCERTAINTY_MEASURE_WITH_UNIT (LENGTH_MEASURE( 1.000000000000000082E-05 ), #44724, 'distance_accuracy_value', 'NONE');
#1016=ADVANCED_BREP_SHAPE_REPRESENTATION ( '', ( #89529, #10728 ), #35180 ) ;
#1085=DIRECTION ( 'NONE',  ( -0.7071067811865460184, 8.659560562354953812E-17, -0.7071067811865490160 ) ) ;
#1178=CIRCLE ( 'NONE', #61525, 8.500000000000000000 ) ;
#1696=CARTESIAN_POINT ( 'NONE',  ( -2.500000000000002220, 1.714505518806294638E-15, -14.00000000000000000 ) ) ;
#1779=AXIS2_PLACEMENT_3D ( 'NONE', #25073, #81145, #33164 ) ;
#1985=DIRECTION ( 'NONE',  ( 0.000000000000000000, 0.000000000000000000, -1.000000000000000000 ) ) ;
#2410=VECTOR ( 'NONE', #80931, 999.9999999999998863 ) ;
#2571=EDGE_CURVE ( 'NONE', #42449, #41982, #85836, .T. ) ;
#2600=CARTESIAN_POINT ( 'NONE',  ( -2.100000000000004530, 1.040949779275250140E-15, -8.500000000000000000 ) ) ;
#3777=VERTEX_POINT ( 'NONE', #74463 ) ;
#4255=SURFACE_STYLE_FILL_AREA ( #19954 ) ;
#4290=ORIENTED_EDGE ( 'NONE', *, *, #2571, .F. ) ;
#4715=DIRECTION ( 'NONE',  ( 0.000000000000000000, 0.000000000000000000, 1.000000000000000000 ) ) ;
#5019=AXIS2_PLACEMENT_3D ( 'NONE', #104458, #30607, #19884 ) ;
#5499=CARTESIAN_POINT ( 'NONE',  ( 0.000000000000000000, 1.714505518806294638E-15, -14.00000000000000000 ) ) ;
#5588=VERTEX_POINT ( 'NONE', #20656 ) ;
#5728=VECTOR ( 'NONE', #70470, 1000.000000000000000 ) ;
#5871=CONICAL_SURFACE ( 'NONE', #41985, 8.900000000000000355, 0.7853981633974418397 ) ;
#6524=CYLINDRICAL_SURFACE ( 'NONE', #11893, 8.500000000000000000 ) ;
#6525=LINE ( 'NONE', #88533, #81085 ) ;
#6589=AXIS2_PLACEMENT_3D ( 'NONE', #16954, #49831, #73564 ) ;
#8409=CONICAL_SURFACE ( 'NONE', #22230, 8.500000000000000000, 0.7853981633974504994 ) ;
#8520=DIRECTION ( 'NONE',  ( 0.000000000000000000, 0.000000000000000000, 1.000000000000000000 ) ) ;
#8556=EDGE_LOOP ( 'NONE', ( #17501, #73272, #94404, #4290 ) ) ;
#8968=PRODUCT_DEFINITION_CONTEXT ( 'detailed design', #38327, 'design' ) ;
#9932=EDGE_LOOP ( 'NONE', ( #48593, #750, #40747, #50229 ) ) ;
#9961=DIRECTION ( 'NONE',  ( -1.000000000000000000, 0.000000000000000000, -0.000000000000000000 ) ) ;
#10728=AXIS2_PLACEMENT_3D ( 'NONE', #14983, #57033, #47878 ) ;
#10986=EDGE_LOOP ( 'NONE', ( #93852, #63174, #60912, #102809 ) ) ;
#11279=SURFACE_STYLE_FILL_AREA ( #78678 ) ;
#11893=AXIS2_PLACEMENT_3D ( 'NONE', #39459, #23281, #24351 ) ;
#11900=DIRECTION ( 'NONE',  ( 0.7071067811865521247, 8.659560562354877391E-17, 0.7071067811865430208 ) ) ;
#11964=DIRECTION ( 'NONE',  ( -1.000000000000000000, -0.000000000000000000, -0.000000000000000000 ) ) ;
#12657=EDGE_LOOP ( 'NONE', ( #24893, #74320, #104654, #25191 ) ) ;
#12740=( GEOMETRIC_REPRESENTATION_CONTEXT ( 3 ) GLOBAL_UNCERTAINTY_ASSIGNED_CONTEXT ( ( #83395 ) ) GLOBAL_UNIT_ASSIGNED_CONTEXT ( ( #43666, #60413, #45800 ) ) REPRESENTATION_CONTEXT ( 'NONE', 'WORKASPACE' ) );
#12817=VERTEX_POINT ( 'NONE', #1696 ) ;
#14091=EDGE_LOOP ( 'NONE', ( #72744, #66382 ) ) ;
#14583=FACE_OUTER_BOUND ( 'NONE', #10986, .T. ) ;
#14983=CARTESIAN_POINT ( 'NONE',  ( 0.000000000000000000, 0.000000000000000000, 0.000000000000000000 ) ) ;
#15645=AXIS2_PLACEMENT_3D ( 'NONE', #50685, #16216, #58272 ) ;
#15902=EDGE_LOOP ( 'NONE', ( #93308, #28305 ) ) ;
#16216=DIRECTION ( 'NONE',  ( -1.000000000000000000, -0.000000000000000000, -0.000000000000000000 ) ) ;
#16515=CARTESIAN_POINT ( 'NONE',  ( -34.92499999999994742, 1.714505518806294638E-15, -14.00000000000000000 ) ) ;
#16954=CARTESIAN_POINT ( 'NONE',  ( -2.500000000000001332, 14.00000000000000000, 0.000000000000000000 ) ) ;
#17367=EDGE_CURVE ( 'NONE', #105711, #24672, #37607, .T. ) ;
#17429=ORIENTED_EDGE ( 'NONE', *, *, #97770, .T. ) ;
#17501=ORIENTED_EDGE ( 'NONE', *, *, #32460, .F. ) ;
#17622=UNCERTAINTY_MEASURE_WITH_UNIT (LENGTH_MEASURE( 1.000000000000000082E-05 ), #94362, 'distance_accuracy_value', 'NONE');
#17624=ADVANCED_FACE ( 'NONE', ( #59598, #92472 ), #18078, .F. ) ;
#17740=CARTESIAN_POINT ( 'NONE',  ( -0.4000000000000045186, 0.000000000000000000, 8.500000000000000000 ) ) ;
#17831=EDGE_CURVE ( 'NONE', #5588, #41982, #32948, .T. ) ;
#18078=PLANE ( 'NONE',  #97113 ) ;
#18760=DIRECTION ( 'NONE',  ( -1.000000000000000000, -0.000000000000000000, -0.000000000000000000 ) ) ;
#19811=LINE ( 'NONE', #101739, #53463 ) ;
#19884=DIRECTION ( 'NONE',  ( 0.000000000000000000, 0.000000000000000000, -1.000000000000000000 ) ) ;
#19954=FILL_AREA_STYLE ('',( #29115 ) ) ;
#20524=( NAMED_UNIT ( * ) SI_UNIT ( $, .STERADIAN. ) SOLID_ANGLE_UNIT ( ) );
#20656=CARTESIAN_POINT ( 'NONE',  ( -0.4000000000000045186, 1.040949779275250140E-15, -8.500000000000000000 ) ) ;
#20801=AXIS2_PLACEMENT_3D ( 'NONE', #62011, #39320, #87336 ) ;
#20905=DIRECTION ( 'NONE',  ( 0.000000000000000000, 0.000000000000000000, 1.000000000000000000 ) ) ;
#22049=SURFACE_STYLE_USAGE ( .BOTH. , #63026 ) ;
#22230=AXIS2_PLACEMENT_3D ( 'NONE', #47492, #39433, #31360 ) ;
#22933=DIRECTION ( 'NONE',  ( 0.000000000000000000, 0.000000000000000000, -1.000000000000000000 ) ) ;
#23281=DIRECTION ( 'NONE',  ( -1.000000000000000000, -0.000000000000000000, -0.000000000000000000 ) ) ;
#23683=DIRECTION ( 'NONE',  ( 0.000000000000000000, 0.000000000000000000, 1.000000000000000000 ) ) ;
#24074=ORIENTED_EDGE ( 'NONE', *, *, #93832, .F. ) ;
#24274=DIRECTION ( 'NONE',  ( 0.000000000000000000, 0.000000000000000000, 1.000000000000000000 ) ) ;
#24351=DIRECTION ( 'NONE',  ( 0.000000000000000000, 0.000000000000000000, 1.000000000000000000 ) ) ;
#24465=CARTESIAN_POINT ( 'NONE',  ( -2.500000000000002220, 0.000000000000000000, 14.00000000000000000 ) ) ;
#24672=VERTEX_POINT ( 'NONE', #24465 ) ;
#24893=ORIENTED_EDGE ( 'NONE', *, *, #26310, .F. ) ;
#25073=CARTESIAN_POINT ( 'NONE',  ( -2.100000000000004530, 0.000000000000000000, 0.000000000000000000 ) ) ;
#25156=CIRCLE ( 'NONE', #68172, 14.00000000000000000 ) ;
#25191=ORIENTED_EDGE ( 'NONE', *, *, #17831, .F. ) ;
#25275=DIRECTION ( 'NONE',  ( -1.000000000000000000, -0.000000000000000000, -0.000000000000000000 ) ) ;
#26310=EDGE_CURVE ( 'NONE', #37464, #5588, #1178, .T. ) ;
#26853=CARTESIAN_POINT ( 'NONE',  ( 0.000000000000000000, 0.000000000000000000, 0.000000000000000000 ) ) ;
#27533=ADVANCED_FACE ( 'NONE', ( #66019, #98899 ), #31564, .F. ) ;
#27534=SURFACE_STYLE_USAGE ( .BOTH. , #61470 ) ;
#27833=ORIENTED_EDGE ( 'NONE', *, *, #93832, .T. ) ;
#27897=DIRECTION ( 'NONE',  ( -1.000000000000000000, -0.000000000000000000, -0.000000000000000000 ) ) ;
#27927=CARTESIAN_POINT ( 'NONE',  ( 0.000000000000000000, 0.000000000000000000, 0.000000000000000000 ) ) ;
#28133=LINE ( 'NONE', #71196, #91193 ) ;
#28204=CARTESIAN_POINT ( 'NONE',  ( -34.92499999999994742, 0.000000000000000000, 0.000000000000000000 ) ) ;
#28305=ORIENTED_EDGE ( 'NONE', *, *, #89175, .T. ) ;
#28585=( NAMED_UNIT ( * ) PLANE_ANGLE_UNIT ( ) SI_UNIT ( $, .RADIAN. ) );
#28697=EDGE_LOOP ( 'NONE', ( #60346, #31466 ) ) ;
#29044=DIRECTION ( 'NONE',  ( 1.000000000000000000, -0.000000000000000000, -0.000000000000000000 ) ) ;
#29115=FILL_AREA_STYLE_COLOUR ( '', #44501 ) ;
#30398=ORIENTED_EDGE ( 'NONE', *, *, #79381, .F. ) ;
#30607=DIRECTION ( 'NONE',  ( 1.000000000000000000, -0.000000000000000000, -0.000000000000000000 ) ) ;
#30731=CIRCLE ( 'NONE', #53114, 8.900000000000000355 ) ;
#30732=ORIENTED_EDGE ( 'NONE', *, *, #47847, .F. ) ;
#31050=AXIS2_PLACEMENT_3D ( 'NONE', #28204, #11964, #62150 ) ;
#31360=DIRECTION ( 'NONE',  ( 0.000000000000000000, 0.000000000000000000, 1.000000000000000000 ) ) ;
#31387=DIRECTION ( 'NONE',  ( -1.000000000000000000, -0.000000000000000000, -0.000000000000000000 ) ) ;
#31466=ORIENTED_EDGE ( 'NONE', *, *, #2571, .T. ) ;
#31564=PLANE ( 'NONE',  #6589 ) ;
#31660=CARTESIAN_POINT ( 'NONE',  ( 0.000000000000000000, 0.000000000000000000, 14.00000000000000000 ) ) ;
#31710=COLOUR_RGB ( '', 0.40784314, 0.44705882, 0.49803922) ;
#32460=EDGE_CURVE ( 'NONE', #37464, #42449, #28133, .T. ) ;
#32678=ADVANCED_FACE ( 'NONE', ( #57125 ), #73303, .T. ) ;
#32948=LINE ( 'NONE', #89568, #2410 ) ;
#32964=FACE_OUTER_BOUND ( 'NONE', #60229, .T. ) ;
#33164=DIRECTION ( 'NONE',  ( 0.000000000000000000, 0.000000000000000000, 1.000000000000000000 ) ) ;
#33818=DIRECTION ( 'NONE',  ( -1.000000000000000000, -0.000000000000000000, -0.000000000000000000 ) ) ;
#34594=CARTESIAN_POINT ( 'NONE',  ( -2.100000000000004530, 1.040949779275250140E-15, -8.500000000000000000 ) ) ;
#34893=DIRECTION ( 'NONE',  ( 0.000000000000000000, 0.000000000000000000, 1.000000000000000000 ) ) ;
#34917=DIRECTION ( 'NONE',  ( -1.000000000000000000, -0.000000000000000000, -0.000000000000000000 ) ) ;
#35180=( GEOMETRIC_REPRESENTATION_CONTEXT ( 3 ) GLOBAL_UNCERTAINTY_ASSIGNED_CONTEXT ( ( #17622 ) ) GLOBAL_UNIT_ASSIGNED_CONTEXT ( ( #94362, #28585, #20524 ) ) REPRESENTATION_CONTEXT ( 'NONE', 'WORKASPACE' ) );
#35472=EDGE_LOOP ( 'NONE', ( #30398, #41674, #405, #17429 ) ) ;
#35835=CARTESIAN_POINT ( 'NONE',  ( -2.100000000000004530, 0.000000000000000000, 0.000000000000000000 ) ) ;
#36265=CIRCLE ( 'NONE', #20801, 14.00000000000000000 ) ;
#36688=FILL_AREA_STYLE_COLOUR ( '', #31710 ) ;
#37287=CARTESIAN_POINT ( 'NONE',  ( 0.000000000000000000, 1.089935651241144357E-15, 8.900000000000000355 ) ) ;
#37464=VERTEX_POINT ( 'NONE', #17740 ) ;
#37607=LINE ( 'NONE', #45146, #5728 ) ;
#37724=( NAMED_UNIT ( * ) SI_UNIT ( $, .STERADIAN. ) SOLID_ANGLE_UNIT ( ) );
#37766=CONICAL_SURFACE ( 'NONE', #5019, 8.900000000000000355, 0.7853981633974418397 ) ;
#37847=CARTESIAN_POINT ( 'NONE',  ( -2.500000000000001332, 0.000000000000000000, 0.000000000000000000 ) ) ;
#38327=APPLICATION_CONTEXT ( 'automotive_design' ) ;
#38688=FACE_OUTER_BOUND ( 'NONE', #8556, .T. ) ;
#39319=AXIS2_PLACEMENT_3D ( 'NONE', #101730, #27897, #79049 ) ;
#39320=DIRECTION ( 'NONE',  ( -1.000000000000000000, -0.000000000000000000, -0.000000000000000000 ) ) ;
#39433=DIRECTION ( 'NONE',  ( -1.000000000000000000, 0.000000000000000000, 0.000000000000000000 ) ) ;
#39459=CARTESIAN_POINT ( 'NONE',  ( -34.92499999999994742, 0.000000000000000000, 0.000000000000000000 ) ) ;
#40747=ORIENTED_EDGE ( 'NONE', *, *, #78643, .F. ) ;
#41674=ORIENTED_EDGE ( 'NONE', *, *, #58086, .T. ) ;
#41797=CARTESIAN_POINT ( 'NONE',  ( 0.000000000000000000, 8.500000000000000000, 0.000000000000000000 ) ) ;
#41982=VERTEX_POINT ( 'NONE', #96293 ) ;
#41985=AXIS2_PLACEMENT_3D ( 'NONE', #26853, #50526, #1985 ) ;
#42449=VERTEX_POINT ( 'NONE', #37287 ) ;
#43666=( LENGTH_UNIT ( ) NAMED_UNIT ( * ) SI_UNIT ( .MILLI., .METRE. ) );
#43880=DIRECTION ( 'NONE',  ( -1.000000000000000000, 0.000000000000000000, 0.000000000000000000 ) ) ;
#44212=PRESENTATION_STYLE_ASSIGNMENT (( #27534 ) ) ;
#44352=CYLINDRICAL_SURFACE ( 'NONE', #31050, 14.00000000000000000 ) ;
#44501=COLOUR_RGB ( '', 0.40784314, 0.44705882, 0.49803922) ;
#44724=( LENGTH_UNIT ( ) NAMED_UNIT ( * ) SI_UNIT ( .MILLI., .METRE. ) );
#45113=DIRECTION ( 'NONE',  ( -0.7071067811865460184, 0.000000000000000000, 0.7071067811865490160 ) ) ;
#45146=CARTESIAN_POINT ( 'NONE',  ( -34.92499999999994742, 0.000000000000000000, 14.00000000000000000 ) ) ;
#45352=ADVANCED_FACE ( 'NONE', ( #38688 ), #37766, .F. ) ;
#45410=EDGE_CURVE ( 'NONE', #105140, #12817, #90412, .T. ) ;
#45485=AXIS2_PLACEMENT_3D ( 'NONE', #85052, #52668, #66736 ) ;
#45800=( NAMED_UNIT ( * ) SI_UNIT ( $, .STERADIAN. ) SOLID_ANGLE_UNIT ( ) );
#46540=CONICAL_SURFACE ( 'NONE', #1779, 8.500000000000000000, 0.7853981633974504994 ) ;
#47325=PRODUCT_DEFINITION_SHAPE ( 'NONE', 'NONE',  #58835 ) ;
#47492=CARTESIAN_POINT ( 'NONE',  ( -2.100000000000004530, 0.000000000000000000, 0.000000000000000000 ) ) ;
#47847=EDGE_CURVE ( 'NONE', #80344, #3777, #53193, .T. ) ;
#47878=DIRECTION ( 'NONE',  ( 1.000000000000000000, 0.000000000000000000, 0.000000000000000000 ) ) ;
#48090=ORIENTED_EDGE ( 'NONE', *, *, #61163, .F. ) ;
#48552=ORIENTED_EDGE ( 'NONE', *, *, #45410, .F. ) ;
#48593=ORIENTED_EDGE ( 'NONE', *, *, #82338, .T. ) ;
#49831=DIRECTION ( 'NONE',  ( 1.000000000000000000, 0.000000000000000000, 0.000000000000000000 ) ) ;
#50229=ORIENTED_EDGE ( 'NONE', *, *, #17367, .F. ) ;
#50406=DIRECTION ( 'NONE',  ( -0.000000000000000000, 0.000000000000000000, 1.000000000000000000 ) ) ;
#50526=DIRECTION ( 'NONE',  ( 1.000000000000000000, -0.000000000000000000, -0.000000000000000000 ) ) ;
#50685=CARTESIAN_POINT ( 'NONE',  ( -34.92499999999994742, 0.000000000000000000, 0.000000000000000000 ) ) ;
#51558=AXIS2_PLACEMENT_3D ( 'NONE', #27927, #94757, #20905 ) ;
#52282=SHAPE_REPRESENTATION_RELATIONSHIP ( 'NONE' , 'NONE' ,  #103287, #1016 ) ;
#52613=EDGE_CURVE ( 'NONE', #53891, #74726, #66933, .T. ) ;
#52668=DIRECTION ( 'NONE',  ( -1.000000000000000000, 0.000000000000000000, 0.000000000000000000 ) ) ;
#53114=AXIS2_PLACEMENT_3D ( 'NONE', #57907, #56848, #22933 ) ;
#53193=LINE ( 'NONE', #71477, #88088 ) ;
#53463=VECTOR ( 'NONE', #34917, 1000.000000000000000 ) ;
#53891=VERTEX_POINT ( 'NONE', #2600 ) ;
#54265=EDGE_CURVE ( 'NONE', #41982, #42449, #91851, .T. ) ;
#55367=DIRECTION ( 'NONE',  ( -1.000000000000000000, -0.000000000000000000, -0.000000000000000000 ) ) ;
#55555=DIRECTION ( 'NONE',  ( 1.000000000000000000, 0.000000000000000000, 0.000000000000000000 ) ) ;
#56848=DIRECTION ( 'NONE',  ( 1.000000000000000000, 0.000000000000000000, 0.000000000000000000 ) ) ;
#56856=ORIENTED_EDGE ( 'NONE', *, *, #82338, .F. ) ;
#57033=DIRECTION ( 'NONE',  ( 0.000000000000000000, 0.000000000000000000, 1.000000000000000000 ) ) ;
#57125=FACE_OUTER_BOUND ( 'NONE', #9932, .T. ) ;
#57907=CARTESIAN_POINT ( 'NONE',  ( -2.500000000000001332, 0.000000000000000000, 0.000000000000000000 ) ) ;
#58057=CARTESIAN_POINT ( 'NONE',  ( 0.000000000000000000, 0.000000000000000000, 0.000000000000000000 ) ) ;
#58086=EDGE_CURVE ( 'NONE', #5588, #37464, #61535, .T. ) ;
#58262=MECHANICAL_DESIGN_GEOMETRIC_PRESENTATION_REPRESENTATION('',(#80896),#94719);
#58272=DIRECTION ( 'NONE',  ( 0.000000000000000000, 0.000000000000000000, 1.000000000000000000 ) ) ;
#58397=CLOSED_SHELL ( 'NONE', ( #72266, #97627, #32678, #69129, #79388, #17624, #91566, #27533, #45352, #76951 ) ) ;
#58835=PRODUCT_DEFINITION ( 'UNKNOWN', '', #73079, #8968 ) ;
#59598=FACE_BOUND ( 'NONE', #28697, .T. ) ;
#60229=EDGE_LOOP ( 'NONE', ( #78489, #61366, #27833, #90158 ) ) ;
#60346=ORIENTED_EDGE ( 'NONE', *, *, #54265, .T. ) ;
#60413=( NAMED_UNIT ( * ) PLANE_ANGLE_UNIT ( ) SI_UNIT ( $, .RADIAN. ) );
#60912=ORIENTED_EDGE ( 'NONE', *, *, #47847, .T. ) ;
#61163=EDGE_CURVE ( 'NONE', #3777, #74726, #30731, .T. ) ;
#61366=ORIENTED_EDGE ( 'NONE', *, *, #79381, .T. ) ;
#61470=SURFACE_SIDE_STYLE ('',( #11279 ) ) ;
#61525=AXIS2_PLACEMENT_3D ( 'NONE', #69976, #29044, #4715 ) ;
#61535=CIRCLE ( 'NONE', #95937, 8.500000000000000000 ) ;
#61724=ORIENTED_EDGE ( 'NONE', *, *, #99929, .F. ) ;
#62011=CARTESIAN_POINT ( 'NONE',  ( -2.500000000000002220, 0.000000000000000000, 0.000000000000000000 ) ) ;
#62150=DIRECTION ( 'NONE',  ( 0.000000000000000000, 0.000000000000000000, 1.000000000000000000 ) ) ;
#63026=SURFACE_SIDE_STYLE ('',( #4255 ) ) ;
#63174=ORIENTED_EDGE ( 'NONE', *, *, #97770, .F. ) ;
#64646=DIRECTION ( 'NONE',  ( 1.000000000000000000, -0.000000000000000000, -0.000000000000000000 ) ) ;
#65234=DIRECTION ( 'NONE',  ( -1.000000000000000000, -0.000000000000000000, -0.000000000000000000 ) ) ;
#66019=FACE_BOUND ( 'NONE', #15902, .T. ) ;
#66382=ORIENTED_EDGE ( 'NONE', *, *, #99929, .T. ) ;
#66559=ORIENTED_EDGE ( 'NONE', *, *, #90069, .F. ) ;
#66736=DIRECTION ( 'NONE',  ( 0.000000000000000000, 0.000000000000000000, -1.000000000000000000 ) ) ;
#66933=LINE ( 'NONE', #34594, #105630 ) ;
#67549=AXIS2_PLACEMENT_3D ( 'NONE', #69936, #18760, #84530 ) ;
#68172=AXIS2_PLACEMENT_3D ( 'NONE', #75381, #25275, #8520 ) ;
#68716=DIRECTION ( 'NONE',  ( 0.000000000000000000, 0.000000000000000000, -1.000000000000000000 ) ) ;
#68883=FACE_OUTER_BOUND ( 'NONE', #12657, .T. ) ;
#69129=ADVANCED_FACE ( 'NONE', ( #32964 ), #6524, .F. ) ;
#69936=CARTESIAN_POINT ( 'NONE',  ( 0.000000000000000000, 0.000000000000000000, 0.000000000000000000 ) ) ;
#69976=CARTESIAN_POINT ( 'NONE',  ( -0.4000000000000045186, 0.000000000000000000, 0.000000000000000000 ) ) ;
#70177=DIRECTION ( 'NONE',  ( 0.000000000000000000, 0.000000000000000000, -1.000000000000000000 ) ) ;
#70470=DIRECTION ( 'NONE',  ( -1.000000000000000000, -0.000000000000000000, -0.000000000000000000 ) ) ;
#71105=PRESENTATION_STYLE_ASSIGNMENT (( #22049 ) ) ;
#71196=CARTESIAN_POINT ( 'NONE',  ( 0.000000000000000000, 1.089935651241144357E-15, 8.900000000000000355 ) ) ;
#71215=CARTESIAN_POINT ( 'NONE',  ( -2.100000000000004530, 0.000000000000000000, 8.500000000000000000 ) ) ;
#71324=CIRCLE ( 'NONE', #45485, 8.500000000000000000 ) ;
#71477=CARTESIAN_POINT ( 'NONE',  ( -2.100000000000004530, 0.000000000000000000, 8.500000000000000000 ) ) ;
#72266=ADVANCED_FACE ( 'NONE', ( #82208 ), #46540, .F. ) ;
#72744=ORIENTED_EDGE ( 'NONE', *, *, #78643, .T. ) ;
#73001=STYLED_ITEM ( 'NONE', ( #44212 ), #1016 ) ;
#73079=PRODUCT_DEFINITION_FORMATION_WITH_SPECIFIED_SOURCE ( 'ANY', '', #101508, .NOT_KNOWN. ) ;
#73272=ORIENTED_EDGE ( 'NONE', *, *, #58086, .F. ) ;
#73303=CYLINDRICAL_SURFACE ( 'NONE', #84405, 14.00000000000000000 ) ;
#73564=DIRECTION ( 'NONE',  ( 0.000000000000000000, 0.000000000000000000, -1.000000000000000000 ) ) ;
#74320=ORIENTED_EDGE ( 'NONE', *, *, #32460, .T. ) ;
#74463=CARTESIAN_POINT ( 'NONE',  ( -2.500000000000001332, 0.000000000000000000, 8.900000000000000355 ) ) ;
#74726=VERTEX_POINT ( 'NONE', #102853 ) ;
#75381=CARTESIAN_POINT ( 'NONE',  ( -2.500000000000002220, 0.000000000000000000, 0.000000000000000000 ) ) ;
#75503=CIRCLE ( 'NONE', #94480, 8.900000000000000355 ) ;
#75650=CIRCLE ( 'NONE', #51558, 14.00000000000000000 ) ;
#76393=ORIENTED_EDGE ( 'NONE', *, *, #52613, .T. ) ;
#76951=ADVANCED_FACE ( 'NONE', ( #14583 ), #8409, .F. ) ;
#77469=VECTOR ( 'NONE', #55367, 1000.000000000000000 ) ;
#77780=FACE_OUTER_BOUND ( 'NONE', #89983, .T. ) ;
#78489=ORIENTED_EDGE ( 'NONE', *, *, #26310, .T. ) ;
#78643=EDGE_CURVE ( 'NONE', #24672, #12817, #36265, .T. ) ;
#78678=FILL_AREA_STYLE ('',( #36688 ) ) ;
#79049=DIRECTION ( 'NONE',  ( 0.000000000000000000, 0.000000000000000000, 1.000000000000000000 ) ) ;
#79381=EDGE_CURVE ( 'NONE', #5588, #53891, #6525, .T. ) ;
#79388=ADVANCED_FACE ( 'NONE', ( #97136 ), #89060, .F. ) ;
#80344=VERTEX_POINT ( 'NONE', #71215 ) ;
#80496=EDGE_CURVE ( 'NONE', #37464, #80344, #19811, .T. ) ;
#80896=STYLED_ITEM ( 'NONE', ( #71105 ), #89529 ) ;
#80931=DIRECTION ( 'NONE',  ( 0.7071067811865521247, 0.000000000000000000, -0.7071067811865430208 ) ) ;
#81042=ORIENTED_EDGE ( 'NONE', *, *, #90069, .T. ) ;
#81065=EDGE_LOOP ( 'NONE', ( #24074, #76393, #48090, #30732 ) ) ;
#81085=VECTOR ( 'NONE', #31387, 1000.000000000000000 ) ;
#81145=DIRECTION ( 'NONE',  ( -1.000000000000000000, 0.000000000000000000, 0.000000000000000000 ) ) ;
#82208=FACE_OUTER_BOUND ( 'NONE', #81065, .T. ) ;
#82338=EDGE_CURVE ( 'NONE', #105711, #105140, #98466, .T. ) ;
#83395=UNCERTAINTY_MEASURE_WITH_UNIT (LENGTH_MEASURE( 1.000000000000000082E-05 ), #43666, 'distance_accuracy_value', 'NONE');
#84405=AXIS2_PLACEMENT_3D ( 'NONE', #106199, #65234, #24274 ) ;
#84530=DIRECTION ( 'NONE',  ( 0.000000000000000000, 0.000000000000000000, 1.000000000000000000 ) ) ;
#85052=CARTESIAN_POINT ( 'NONE',  ( -2.100000000000004530, 0.000000000000000000, 0.000000000000000000 ) ) ;
#85115=MECHANICAL_DESIGN_GEOMETRIC_PRESENTATION_REPRESENTATION('',(#73001),#12740);
#85836=CIRCLE ( 'NONE', #39319, 8.900000000000000355 ) ;
#87336=DIRECTION ( 'NONE',  ( 0.000000000000000000, 0.000000000000000000, 1.000000000000000000 ) ) ;
#88088=VECTOR ( 'NONE', #45113, 1000.000000000000114 ) ;
#88400=AXIS2_PLACEMENT_3D ( 'NONE', #58057, #33818, #34893 ) ;
#88533=CARTESIAN_POINT ( 'NONE',  ( -34.92499999999994742, 1.040949779275250140E-15, -8.500000000000000000 ) ) ;
#88869=ORIENTED_EDGE ( 'NONE', *, *, #17367, .T. ) ;
#89060=CYLINDRICAL_SURFACE ( 'NONE', #15645, 8.500000000000000000 ) ;
#89175=EDGE_CURVE ( 'NONE', #74726, #3777, #75503, .T. ) ;
#89529=MANIFOLD_SOLID_BREP ( 'IDChamferFar', #58397 ) ;
#89568=CARTESIAN_POINT ( 'NONE',  ( 0.000000000000000000, 0.000000000000000000, -8.900000000000000355 ) ) ;
#89983=EDGE_LOOP ( 'NONE', ( #48552, #81042, #88869, #61724 ) ) ;
#90069=EDGE_CURVE ( 'NONE', #105140, #105711, #75650, .T. ) ;
#90158=ORIENTED_EDGE ( 'NONE', *, *, #80496, .F. ) ;
#90412=LINE ( 'NONE', #16515, #77469 ) ;
#91193=VECTOR ( 'NONE', #11900, 999.9999999999998863 ) ;
#91566=ADVANCED_FACE ( 'NONE', ( #77780 ), #44352, .T. ) ;
#91684=CIRCLE ( 'NONE', #95151, 8.500000000000000000 ) ;
#91851=CIRCLE ( 'NONE', #88400, 8.900000000000000355 ) ;
#92472=FACE_OUTER_BOUND ( 'NONE', #100767, .T. ) ;
#93308=ORIENTED_EDGE ( 'NONE', *, *, #61163, .T. ) ;
#93832=EDGE_CURVE ( 'NONE', #53891, #80344, #91684, .T. ) ;
#93852=ORIENTED_EDGE ( 'NONE', *, *, #52613, .F. ) ;
#94362=( LENGTH_UNIT ( ) NAMED_UNIT ( * ) SI_UNIT ( .MILLI., .METRE. ) );
#94404=ORIENTED_EDGE ( 'NONE', *, *, #17831, .T. ) ;
#94480=AXIS2_PLACEMENT_3D ( 'NONE', #37847, #55555, #70177 ) ;
#94719=( GEOMETRIC_REPRESENTATION_CONTEXT ( 3 ) GLOBAL_UNCERTAINTY_ASSIGNED_CONTEXT ( ( #983 ) ) GLOBAL_UNIT_ASSIGNED_CONTEXT ( ( #44724, #94874, #37724 ) ) REPRESENTATION_CONTEXT ( 'NONE', 'WORKASPACE' ) );
#94757=DIRECTION ( 'NONE',  ( -1.000000000000000000, -0.000000000000000000, -0.000000000000000000 ) ) ;
#94869=APPLICATION_CONTEXT ( 'automotive_design' ) ;
#94874=( NAMED_UNIT ( * ) PLANE_ANGLE_UNIT ( ) SI_UNIT ( $, .RADIAN. ) );
#95151=AXIS2_PLACEMENT_3D ( 'NONE', #35835, #43880, #68716 ) ;
#95937=AXIS2_PLACEMENT_3D ( 'NONE', #105625, #64646, #23683 ) ;
#96293=CARTESIAN_POINT ( 'NONE',  ( 0.000000000000000000, 0.000000000000000000, -8.900000000000000355 ) ) ;
#97113=AXIS2_PLACEMENT_3D ( 'NONE', #41797, #9961, #50406 ) ;
#97136=FACE_OUTER_BOUND ( 'NONE', #35472, .T. ) ;
#97627=ADVANCED_FACE ( 'NONE', ( #68883 ), #5871, .F. ) ;
#97770=EDGE_CURVE ( 'NONE', #80344, #53891, #71324, .T. ) ;
#98466=CIRCLE ( 'NONE', #67549, 14.00000000000000000 ) ;
#98899=FACE_OUTER_BOUND ( 'NONE', #14091, .T. ) ;
#99929=EDGE_CURVE ( 'NONE', #12817, #24672, #25156, .T. ) ;
#100767=EDGE_LOOP ( 'NONE', ( #56856, #66559 ) ) ;
#101508=PRODUCT ( 'plain washer hardened small grade a_din_Washer DIN 433 - 17 - 300HV', 'plain washer hardened small grade a_din_Washer DIN 433 - 17 - 300HV', '', ( #103767 ) ) ;
#101730=CARTESIAN_POINT ( 'NONE',  ( 0.000000000000000000, 0.000000000000000000, 0.000000000000000000 ) ) ;
#101739=CARTESIAN_POINT ( 'NONE',  ( -34.92499999999994742, 0.000000000000000000, 8.500000000000000000 ) ) ;
#102809=ORIENTED_EDGE ( 'NONE', *, *, #89175, .F. ) ;
#102853=CARTESIAN_POINT ( 'NONE',  ( -2.500000000000001332, 1.089935651241144160E-15, -8.900000000000000355 ) ) ;
#103246=SHAPE_DEFINITION_REPRESENTATION ( #47325, #103287 ) ;
#103287=SHAPE_REPRESENTATION ( 'plain washer hardened small grade a_din_Washer DIN 433 - 17 - 300HV', ( #10728 ), #35180 ) ;
#103767=PRODUCT_CONTEXT ( 'NONE', #94869, 'mechanical' ) ;
#104458=CARTESIAN_POINT ( 'NONE',  ( 0.000000000000000000, 0.000000000000000000, 0.000000000000000000 ) ) ;
#104654=ORIENTED_EDGE ( 'NONE', *, *, #54265, .F. ) ;
#105140=VERTEX_POINT ( 'NONE', #5499 ) ;
#105625=CARTESIAN_POINT ( 'NONE',  ( -0.4000000000000045186, 0.000000000000000000, 0.000000000000000000 ) ) ;
#105630=VECTOR ( 'NONE', #1085, 1000.000000000000114 ) ;
#105711=VERTEX_POINT ( 'NONE', #31660 ) ;
#106199=CARTESIAN_POINT ( 'NONE',  ( -34.92499999999994742, 0.000000000000000000, 0.000000000000000000 ) ) ;
ENDSEC;
END-ISO-10303-21;
